ISO-10303-21;
HEADER;
/* Generated by software containing ST-Developer
 * from STEP Tools, Inc. (www.steptools.com) 
 */

FILE_DESCRIPTION(
/* description */ ('Ball-type isolation valve (generic)'),
/* implementation_level */ '2;1');

FILE_NAME(
/* name */ 'M4x10 Cap Screw.step',
/* time_stamp */ '2026-10-27T10:53:05-07:00',
/* author */ (''),
/* organization */ (''),
/* preprocessor_version */ 'ST-DEVELOPER v20.2',
/* originating_system */ 'Autodesk Translation Framework v15.17.0.0',
/* authorisation */ '');

FILE_SCHEMA (('AUTOMOTIVE_DESIGN { 1 0 10303 214 3 1 1 }'));
ENDSEC;

DATA;
#10=MECHANICAL_DESIGN_GEOMETRIC_PRESENTATION_REPRESENTATION('',(#302),#7425);
#215=CONICAL_SURFACE('',#4877,0.325,0.785398163397448);
#216=CONICAL_SURFACE('',#4881,0.335,0.785398163397448);
#217=CONICAL_SURFACE('',#4885,0.21,0.463647609000806);
#220=ORIENTED_CLOSED_SHELL('',*,#4109,.F.);
#223=BREP_WITH_VOIDS('Body1',#4110,(#220));
#250=SHAPE_REPRESENTATION_RELATIONSHIP('SRR','None',#7561,#276);
#276=ADVANCED_BREP_SHAPE_REPRESENTATION('',(#223),#7424);
#302=STYLED_ITEM('',(#7751),#223);
#418=FACE_BOUND('',#1162,.T.);
#568=PLANE('',#4865);
#569=PLANE('',#4866);
#570=PLANE('',#4867);
#571=PLANE('',#4868);
#572=PLANE('',#4869);
#573=PLANE('',#4870);
#574=PLANE('',#4871);
#575=PLANE('',#4872);
#576=PLANE('',#4873);
#577=PLANE('',#4875);
#578=PLANE('',#4883);
#812=FACE_OUTER_BOUND('',#1148,.T.);
#813=FACE_OUTER_BOUND('',#1149,.T.);
#814=FACE_OUTER_BOUND('',#1150,.T.);
#815=FACE_OUTER_BOUND('',#1151,.T.);
#816=FACE_OUTER_BOUND('',#1152,.T.);
#817=FACE_OUTER_BOUND('',#1153,.T.);
#818=FACE_OUTER_BOUND('',#1154,.T.);
#819=FACE_OUTER_BOUND('',#1155,.T.);
#820=FACE_OUTER_BOUND('',#1156,.T.);
#821=FACE_OUTER_BOUND('',#1157,.T.);
#822=FACE_OUTER_BOUND('',#1158,.T.);
#823=FACE_OUTER_BOUND('',#1159,.T.);
#824=FACE_OUTER_BOUND('',#1160,.T.);
#825=FACE_OUTER_BOUND('',#1161,.T.);
#826=FACE_OUTER_BOUND('',#1163,.T.);
#827=FACE_OUTER_BOUND('',#1164,.T.);
#1148=EDGE_LOOP('',(#3705,#3706,#3707,#3708));
#1149=EDGE_LOOP('',(#3709,#3710,#3711,#3712));
#1150=EDGE_LOOP('',(#3713,#3714,#3715,#3716));
#1151=EDGE_LOOP('',(#3717,#3718,#3719,#3720));
#1152=EDGE_LOOP('',(#3721,#3722,#3723,#3724));
#1153=EDGE_LOOP('',(#3725,#3726,#3727,#3728));
#1154=EDGE_LOOP('',(#3729,#3730,#3731,#3732,#3733,#3734));
#1155=EDGE_LOOP('',(#3735,#3736,#3737,#3738,#3739,#3740));
#1156=EDGE_LOOP('',(#3741));
#1157=EDGE_LOOP('',(#3742));
#1158=EDGE_LOOP('',(#3743,#3744,#3745,#3746));
#1159=EDGE_LOOP('',(#3747,#3748,#3749,#3750));
#1160=EDGE_LOOP('',(#3751,#3752,#3753,#3754));
#1161=EDGE_LOOP('',(#3755));
#1162=EDGE_LOOP('',(#3756));
#1163=EDGE_LOOP('',(#3757,#3758,#3759,#3760));
#1164=EDGE_LOOP('',(#3761,#3762,#3763,#3764));
#1450=LINE('',#7296,#1758);
#1451=LINE('',#7298,#1759);
#1452=LINE('',#7300,#1760);
#1453=LINE('',#7301,#1761);
#1454=LINE('',#7304,#1762);
#1455=LINE('',#7306,#1763);
#1456=LINE('',#7307,#1764);
#1457=LINE('',#7310,#1765);
#1458=LINE('',#7312,#1766);
#1459=LINE('',#7313,#1767);
#1460=LINE('',#7316,#1768);
#1461=LINE('',#7318,#1769);
#1462=LINE('',#7319,#1770);
#1463=LINE('',#7322,#1771);
#1464=LINE('',#7324,#1772);
#1465=LINE('',#7325,#1773);
#1466=LINE('',#7327,#1774);
#1467=LINE('',#7328,#1775);
#1468=LINE('',#7340,#1776);
#1469=LINE('',#7344,#1777);
#1470=LINE('',#7348,#1778);
#1471=LINE('',#7355,#1779);
#1472=LINE('',#7357,#1780);
#1758=VECTOR('',#6117,1.);
#1759=VECTOR('',#6118,1.);
#1760=VECTOR('',#6119,1.);
#1761=VECTOR('',#6120,1.);
#1762=VECTOR('',#6123,1.);
#1763=VECTOR('',#6124,1.);
#1764=VECTOR('',#6125,1.);
#1765=VECTOR('',#6128,1.);
#1766=VECTOR('',#6129,1.);
#1767=VECTOR('',#6130,1.);
#1768=VECTOR('',#6133,1.);
#1769=VECTOR('',#6134,1.);
#1770=VECTOR('',#6135,1.);
#1771=VECTOR('',#6138,1.);
#1772=VECTOR('',#6139,1.);
#1773=VECTOR('',#6140,1.);
#1774=VECTOR('',#6143,1.);
#1775=VECTOR('',#6144,1.);
#1776=VECTOR('',#6161,0.325);
#1777=VECTOR('',#6166,0.35);
#1778=VECTOR('',#6171,0.335);
#1779=VECTOR('',#6180,0.21);
#1780=VECTOR('',#6183,0.2);
#1949=CIRCLE('',#4874,0.1954);
#1950=CIRCLE('',#4876,0.3);
#1951=CIRCLE('',#4878,0.35);
#1952=CIRCLE('',#4880,0.35);
#1953=CIRCLE('',#4882,0.32);
#1954=CIRCLE('',#4884,0.22);
#1955=CIRCLE('',#4886,0.1954);
#2261=VERTEX_POINT('',#7294);
#2262=VERTEX_POINT('',#7295);
#2263=VERTEX_POINT('',#7297);
#2264=VERTEX_POINT('',#7299);
#2265=VERTEX_POINT('',#7303);
#2266=VERTEX_POINT('',#7305);
#2267=VERTEX_POINT('',#7309);
#2268=VERTEX_POINT('',#7311);
#2269=VERTEX_POINT('',#7315);
#2270=VERTEX_POINT('',#7317);
#2271=VERTEX_POINT('',#7321);
#2272=VERTEX_POINT('',#7323);
#2273=VERTEX_POINT('',#7332);
#2274=VERTEX_POINT('',#7335);
#2275=VERTEX_POINT('',#7338);
#2276=VERTEX_POINT('',#7342);
#2277=VERTEX_POINT('',#7346);
#2278=VERTEX_POINT('',#7350);
#2279=VERTEX_POINT('',#7353);
#2745=EDGE_CURVE('',#2261,#2262,#1450,.T.);
#2746=EDGE_CURVE('',#2262,#2263,#1451,.T.);
#2747=EDGE_CURVE('',#2263,#2264,#1452,.T.);
#2748=EDGE_CURVE('',#2261,#2264,#1453,.T.);
#2749=EDGE_CURVE('',#2262,#2265,#1454,.T.);
#2750=EDGE_CURVE('',#2265,#2266,#1455,.T.);
#2751=EDGE_CURVE('',#2266,#2263,#1456,.T.);
#2752=EDGE_CURVE('',#2265,#2267,#1457,.T.);
#2753=EDGE_CURVE('',#2267,#2268,#1458,.T.);
#2754=EDGE_CURVE('',#2268,#2266,#1459,.T.);
#2755=EDGE_CURVE('',#2267,#2269,#1460,.T.);
#2756=EDGE_CURVE('',#2269,#2270,#1461,.T.);
#2757=EDGE_CURVE('',#2270,#2268,#1462,.T.);
#2758=EDGE_CURVE('',#2269,#2271,#1463,.T.);
#2759=EDGE_CURVE('',#2271,#2272,#1464,.T.);
#2760=EDGE_CURVE('',#2272,#2270,#1465,.T.);
#2761=EDGE_CURVE('',#2271,#2261,#1466,.T.);
#2762=EDGE_CURVE('',#2264,#2272,#1467,.T.);
#2763=EDGE_CURVE('',#2273,#2273,#1949,.T.);
#2764=EDGE_CURVE('',#2274,#2274,#1950,.T.);
#2765=EDGE_CURVE('',#2275,#2275,#1951,.T.);
#2766=EDGE_CURVE('',#2275,#2274,#1468,.T.);
#2767=EDGE_CURVE('',#2276,#2276,#1952,.T.);
#2768=EDGE_CURVE('',#2276,#2275,#1469,.T.);
#2769=EDGE_CURVE('',#2277,#2277,#1953,.T.);
#2770=EDGE_CURVE('',#2277,#2276,#1470,.T.);
#2771=EDGE_CURVE('',#2278,#2278,#1954,.T.);
#2772=EDGE_CURVE('',#2279,#2279,#1955,.F.);
#2773=EDGE_CURVE('',#2279,#2278,#1471,.T.);
#2774=EDGE_CURVE('',#2273,#2279,#1472,.T.);
#3705=ORIENTED_EDGE('',*,*,#2745,.T.);
#3706=ORIENTED_EDGE('',*,*,#2746,.T.);
#3707=ORIENTED_EDGE('',*,*,#2747,.T.);
#3708=ORIENTED_EDGE('',*,*,#2748,.F.);
#3709=ORIENTED_EDGE('',*,*,#2749,.T.);
#3710=ORIENTED_EDGE('',*,*,#2750,.T.);
#3711=ORIENTED_EDGE('',*,*,#2751,.T.);
#3712=ORIENTED_EDGE('',*,*,#2746,.F.);
#3713=ORIENTED_EDGE('',*,*,#2752,.T.);
#3714=ORIENTED_EDGE('',*,*,#2753,.T.);
#3715=ORIENTED_EDGE('',*,*,#2754,.T.);
#3716=ORIENTED_EDGE('',*,*,#2750,.F.);
#3717=ORIENTED_EDGE('',*,*,#2755,.T.);
#3718=ORIENTED_EDGE('',*,*,#2756,.T.);
#3719=ORIENTED_EDGE('',*,*,#2757,.T.);
#3720=ORIENTED_EDGE('',*,*,#2753,.F.);
#3721=ORIENTED_EDGE('',*,*,#2758,.T.);
#3722=ORIENTED_EDGE('',*,*,#2759,.T.);
#3723=ORIENTED_EDGE('',*,*,#2760,.T.);
#3724=ORIENTED_EDGE('',*,*,#2756,.F.);
#3725=ORIENTED_EDGE('',*,*,#2761,.T.);
#3726=ORIENTED_EDGE('',*,*,#2748,.T.);
#3727=ORIENTED_EDGE('',*,*,#2762,.T.);
#3728=ORIENTED_EDGE('',*,*,#2759,.F.);
#3729=ORIENTED_EDGE('',*,*,#2761,.F.);
#3730=ORIENTED_EDGE('',*,*,#2758,.F.);
#3731=ORIENTED_EDGE('',*,*,#2755,.F.);
#3732=ORIENTED_EDGE('',*,*,#2752,.F.);
#3733=ORIENTED_EDGE('',*,*,#2749,.F.);
#3734=ORIENTED_EDGE('',*,*,#2745,.F.);
#3735=ORIENTED_EDGE('',*,*,#2762,.F.);
#3736=ORIENTED_EDGE('',*,*,#2747,.F.);
#3737=ORIENTED_EDGE('',*,*,#2751,.F.);
#3738=ORIENTED_EDGE('',*,*,#2754,.F.);
#3739=ORIENTED_EDGE('',*,*,#2757,.F.);
#3740=ORIENTED_EDGE('',*,*,#2760,.F.);
#3741=ORIENTED_EDGE('',*,*,#2763,.F.);
#3742=ORIENTED_EDGE('',*,*,#2764,.F.);
#3743=ORIENTED_EDGE('',*,*,#2765,.F.);
#3744=ORIENTED_EDGE('',*,*,#2766,.T.);
#3745=ORIENTED_EDGE('',*,*,#2764,.T.);
#3746=ORIENTED_EDGE('',*,*,#2766,.F.);
#3747=ORIENTED_EDGE('',*,*,#2767,.F.);
#3748=ORIENTED_EDGE('',*,*,#2768,.T.);
#3749=ORIENTED_EDGE('',*,*,#2765,.T.);
#3750=ORIENTED_EDGE('',*,*,#2768,.F.);
#3751=ORIENTED_EDGE('',*,*,#2769,.F.);
#3752=ORIENTED_EDGE('',*,*,#2770,.T.);
#3753=ORIENTED_EDGE('',*,*,#2767,.T.);
#3754=ORIENTED_EDGE('',*,*,#2770,.F.);
#3755=ORIENTED_EDGE('',*,*,#2769,.T.);
#3756=ORIENTED_EDGE('',*,*,#2771,.F.);
#3757=ORIENTED_EDGE('',*,*,#2772,.F.);
#3758=ORIENTED_EDGE('',*,*,#2773,.T.);
#3759=ORIENTED_EDGE('',*,*,#2771,.T.);
#3760=ORIENTED_EDGE('',*,*,#2773,.F.);
#3761=ORIENTED_EDGE('',*,*,#2763,.T.);
#3762=ORIENTED_EDGE('',*,*,#2774,.T.);
#3763=ORIENTED_EDGE('',*,*,#2772,.T.);
#3764=ORIENTED_EDGE('',*,*,#2774,.F.);
#3831=CYLINDRICAL_SURFACE('',#4879,0.35);
#3832=CYLINDRICAL_SURFACE('',#4887,0.1954);
#4066=ADVANCED_FACE('',(#812),#568,.F.);
#4067=ADVANCED_FACE('',(#813),#569,.F.);
#4068=ADVANCED_FACE('',(#814),#570,.F.);
#4069=ADVANCED_FACE('',(#815),#571,.F.);
#4070=ADVANCED_FACE('',(#816),#572,.F.);
#4071=ADVANCED_FACE('',(#817),#573,.F.);
#4072=ADVANCED_FACE('',(#818),#574,.F.);
#4073=ADVANCED_FACE('',(#819),#575,.F.);
#4074=ADVANCED_FACE('',(#820),#576,.F.);
#4075=ADVANCED_FACE('',(#821),#577,.T.);
#4076=ADVANCED_FACE('',(#822),#215,.T.);
#4077=ADVANCED_FACE('',(#823),#3831,.T.);
#4078=ADVANCED_FACE('',(#824),#216,.T.);
#4079=ADVANCED_FACE('',(#825,#418),#578,.T.);
#4080=ADVANCED_FACE('',(#826),#217,.T.);
#4081=ADVANCED_FACE('',(#827),#3832,.T.);
#4109=CLOSED_SHELL('',(#4066,#4067,#4068,#4069,#4070,#4071,#4072,#4073));
#4110=CLOSED_SHELL('',(#4074,#4075,#4076,#4077,#4078,#4079,#4080,#4081));
#4864=AXIS2_PLACEMENT_3D('',#7292,#6113,#6114);
#4865=AXIS2_PLACEMENT_3D('',#7293,#6115,#6116);
#4866=AXIS2_PLACEMENT_3D('',#7302,#6121,#6122);
#4867=AXIS2_PLACEMENT_3D('',#7308,#6126,#6127);
#4868=AXIS2_PLACEMENT_3D('',#7314,#6131,#6132);
#4869=AXIS2_PLACEMENT_3D('',#7320,#6136,#6137);
#4870=AXIS2_PLACEMENT_3D('',#7326,#6141,#6142);
#4871=AXIS2_PLACEMENT_3D('',#7329,#6145,#6146);
#4872=AXIS2_PLACEMENT_3D('',#7330,#6147,#6148);
#4873=AXIS2_PLACEMENT_3D('',#7331,#6149,#6150);
#4874=AXIS2_PLACEMENT_3D('',#7333,#6151,#6152);
#4875=AXIS2_PLACEMENT_3D('',#7334,#6153,#6154);
#4876=AXIS2_PLACEMENT_3D('',#7336,#6155,#6156);
#4877=AXIS2_PLACEMENT_3D('',#7337,#6157,#6158);
#4878=AXIS2_PLACEMENT_3D('',#7339,#6159,#6160);
#4879=AXIS2_PLACEMENT_3D('',#7341,#6162,#6163);
#4880=AXIS2_PLACEMENT_3D('',#7343,#6164,#6165);
#4881=AXIS2_PLACEMENT_3D('',#7345,#6167,#6168);
#4882=AXIS2_PLACEMENT_3D('',#7347,#6169,#6170);
#4883=AXIS2_PLACEMENT_3D('',#7349,#6172,#6173);
#4884=AXIS2_PLACEMENT_3D('',#7351,#6174,#6175);
#4885=AXIS2_PLACEMENT_3D('',#7352,#6176,#6177);
#4886=AXIS2_PLACEMENT_3D('',#7354,#6178,#6179);
#4887=AXIS2_PLACEMENT_3D('',#7356,#6181,#6182);
#6113=DIRECTION('axis',(0.,0.,1.));
#6114=DIRECTION('refdir',(1.,0.,0.));
#6115=DIRECTION('center_axis',(0.866025403784439,0.,-0.5));
#6116=DIRECTION('ref_axis',(0.5,0.,0.866025403784439));
#6117=DIRECTION('',(-0.5,0.,-0.866025403784439));
#6118=DIRECTION('',(0.,-1.,0.));
#6119=DIRECTION('',(0.5,0.,0.866025403784439));
#6120=DIRECTION('',(0.,-1.,0.));
#6121=DIRECTION('center_axis',(1.60246890531964E-16,0.,-1.));
#6122=DIRECTION('ref_axis',(1.,0.,1.60246890531964E-16));
#6123=DIRECTION('',(-1.,0.,-1.60246890531964E-16));
#6124=DIRECTION('',(0.,-1.,0.));
#6125=DIRECTION('',(1.,0.,1.60246890531964E-16));
#6126=DIRECTION('center_axis',(-0.866025403784439,0.,-0.5));
#6127=DIRECTION('ref_axis',(0.5,0.,-0.866025403784439));
#6128=DIRECTION('',(-0.5,0.,0.866025403784439));
#6129=DIRECTION('',(0.,-1.,0.));
#6130=DIRECTION('',(0.5,0.,-0.866025403784439));
#6131=DIRECTION('center_axis',(-0.866025403784439,0.,0.5));
#6132=DIRECTION('ref_axis',(-0.5,0.,-0.866025403784439));
#6133=DIRECTION('',(0.5,0.,0.866025403784439));
#6134=DIRECTION('',(0.,-1.,0.));
#6135=DIRECTION('',(-0.5,0.,-0.866025403784439));
#6136=DIRECTION('center_axis',(-1.60246890531964E-16,0.,1.));
#6137=DIRECTION('ref_axis',(-1.,0.,-1.60246890531964E-16));
#6138=DIRECTION('',(1.,0.,1.60246890531964E-16));
#6139=DIRECTION('',(0.,-1.,0.));
#6140=DIRECTION('',(-1.,0.,-1.60246890531964E-16));
#6141=DIRECTION('center_axis',(0.866025403784439,0.,0.5));
#6142=DIRECTION('ref_axis',(-0.5,0.,0.866025403784439));
#6143=DIRECTION('',(0.5,0.,-0.866025403784439));
#6144=DIRECTION('',(-0.5,0.,0.866025403784439));
#6145=DIRECTION('center_axis',(0.,1.,0.));
#6146=DIRECTION('ref_axis',(1.,0.,0.));
#6147=DIRECTION('center_axis',(0.,-1.,0.));
#6148=DIRECTION('ref_axis',(0.,0.,-1.));
#6149=DIRECTION('center_axis',(0.,1.,0.));
#6150=DIRECTION('ref_axis',(1.,0.,0.));
#6151=DIRECTION('center_axis',(0.,1.,0.));
#6152=DIRECTION('ref_axis',(1.,0.,0.));
#6153=DIRECTION('center_axis',(0.,1.,0.));
#6154=DIRECTION('ref_axis',(0.,0.,1.));
#6155=DIRECTION('center_axis',(0.,-1.,0.));
#6156=DIRECTION('ref_axis',(1.,0.,0.));
#6157=DIRECTION('center_axis',(0.,-1.,0.));
#6158=DIRECTION('ref_axis',(1.,0.,0.));
#6159=DIRECTION('center_axis',(0.,-1.,0.));
#6160=DIRECTION('ref_axis',(1.,0.,0.));
#6161=DIRECTION('',(0.707106781186547,0.707106781186548,8.65956056235493E-17));
#6162=DIRECTION('center_axis',(0.,-1.,0.));
#6163=DIRECTION('ref_axis',(1.,0.,0.));
#6164=DIRECTION('center_axis',(0.,-1.,0.));
#6165=DIRECTION('ref_axis',(1.,0.,0.));
#6166=DIRECTION('',(0.,1.,0.));
#6167=DIRECTION('center_axis',(0.,1.,0.));
#6168=DIRECTION('ref_axis',(1.,0.,0.));
#6169=DIRECTION('center_axis',(0.,-1.,0.));
#6170=DIRECTION('ref_axis',(1.,0.,0.));
#6171=DIRECTION('',(-0.707106781186547,0.707106781186548,-8.65956056235493E-17));
#6172=DIRECTION('center_axis',(0.,-1.,0.));
#6173=DIRECTION('ref_axis',(0.,0.,-1.));
#6174=DIRECTION('center_axis',(0.,-1.,0.));
#6175=DIRECTION('ref_axis',(1.,0.,0.));
#6176=DIRECTION('center_axis',(0.,1.,0.));
#6177=DIRECTION('ref_axis',(1.,0.,0.));
#6178=DIRECTION('center_axis',(0.,1.,0.));
#6179=DIRECTION('ref_axis',(1.,0.,0.));
#6180=DIRECTION('',(-0.447213595499958,0.894427190999916,-5.47678698264203E-17));
#6181=DIRECTION('center_axis',(0.,-1.,0.));
#6182=DIRECTION('ref_axis',(1.,0.,0.));
#6183=DIRECTION('',(0.,1.,0.));
#7292=CARTESIAN_POINT('',(0.,0.,0.));
#7293=CARTESIAN_POINT('Origin',(0.0866025403784439,-0.4,-0.15));
#7294=CARTESIAN_POINT('',(0.173205080756888,-0.4,0.));
#7295=CARTESIAN_POINT('',(0.0866025403784439,-0.4,-0.15));
#7296=CARTESIAN_POINT('',(0.173205080756888,-0.4,0.));
#7297=CARTESIAN_POINT('',(0.0866025403784439,-0.64,-0.15));
#7298=CARTESIAN_POINT('',(0.0866025403784439,-0.4,-0.15));
#7299=CARTESIAN_POINT('',(0.173205080756888,-0.64,0.));
#7300=CARTESIAN_POINT('',(0.173205080756888,-0.64,0.));
#7301=CARTESIAN_POINT('',(0.173205080756888,-0.4,0.));
#7302=CARTESIAN_POINT('Origin',(-0.0866025403784438,-0.4,-0.15));
#7303=CARTESIAN_POINT('',(-0.0866025403784438,-0.4,-0.15));
#7304=CARTESIAN_POINT('',(0.0866025403784439,-0.4,-0.15));
#7305=CARTESIAN_POINT('',(-0.0866025403784438,-0.64,-0.15));
#7306=CARTESIAN_POINT('',(-0.0866025403784438,-0.4,-0.15));
#7307=CARTESIAN_POINT('',(0.0866025403784439,-0.64,-0.15));
#7308=CARTESIAN_POINT('Origin',(-0.173205080756888,-0.4,-2.77555756156289E-17));
#7309=CARTESIAN_POINT('',(-0.173205080756888,-0.4,-2.12115047744981E-17));
#7310=CARTESIAN_POINT('',(-0.0866025403784438,-0.4,-0.15));
#7311=CARTESIAN_POINT('',(-0.173205080756888,-0.64,-2.77555756156289E-17));
#7312=CARTESIAN_POINT('',(-0.173205080756888,-0.4,-2.12115047744981E-17));
#7313=CARTESIAN_POINT('',(-0.0866025403784438,-0.64,-0.15));
#7314=CARTESIAN_POINT('Origin',(-0.0866025403784439,-0.4,0.15));
#7315=CARTESIAN_POINT('',(-0.0866025403784439,-0.4,0.15));
#7316=CARTESIAN_POINT('',(-0.173205080756888,-0.4,-2.12115047744981E-17));
#7317=CARTESIAN_POINT('',(-0.0866025403784439,-0.64,0.15));
#7318=CARTESIAN_POINT('',(-0.0866025403784439,-0.4,0.15));
#7319=CARTESIAN_POINT('',(-0.173205080756888,-0.64,-2.12115047744981E-17));
#7320=CARTESIAN_POINT('Origin',(0.0866025403784439,-0.4,0.15));
#7321=CARTESIAN_POINT('',(0.0866025403784439,-0.4,0.15));
#7322=CARTESIAN_POINT('',(-0.0866025403784439,-0.4,0.15));
#7323=CARTESIAN_POINT('',(0.0866025403784439,-0.64,0.15));
#7324=CARTESIAN_POINT('',(0.0866025403784439,-0.4,0.15));
#7325=CARTESIAN_POINT('',(-0.0866025403784439,-0.64,0.15));
#7326=CARTESIAN_POINT('Origin',(0.173205080756888,-0.4,0.));
#7327=CARTESIAN_POINT('',(0.0866025403784439,-0.4,0.15));
#7328=CARTESIAN_POINT('',(0.0866025403784439,-0.64,0.15));
#7329=CARTESIAN_POINT('Origin',(0.,-0.4,-2.77555756156289E-17));
#7330=CARTESIAN_POINT('Origin',(0.,-0.64,-2.77555756156289E-17));
#7331=CARTESIAN_POINT('Origin',(0.,-1.,0.));
#7332=CARTESIAN_POINT('',(-0.1954,-1.,2.39295984553393E-17));
#7333=CARTESIAN_POINT('Origin',(0.,-1.,0.));
#7334=CARTESIAN_POINT('Origin',(0.3,0.4,0.));
#7335=CARTESIAN_POINT('',(-0.3,0.4,-3.67394039744206E-17));
#7336=CARTESIAN_POINT('Origin',(0.,0.4,0.));
#7337=CARTESIAN_POINT('Origin',(0.,0.375,0.));
#7338=CARTESIAN_POINT('',(-0.35,0.35,-4.28626379701573E-17));
#7339=CARTESIAN_POINT('Origin',(0.,0.35,0.));
#7340=CARTESIAN_POINT('',(-0.325,0.375,-3.9801020972289E-17));
#7341=CARTESIAN_POINT('Origin',(0.,0.19,0.));
#7342=CARTESIAN_POINT('',(-0.35,0.03,-4.28626379701574E-17));
#7343=CARTESIAN_POINT('Origin',(0.,0.03,0.));
#7344=CARTESIAN_POINT('',(-0.35,0.19,-4.28626379701574E-17));
#7345=CARTESIAN_POINT('Origin',(0.,0.0149999999999999,0.));
#7346=CARTESIAN_POINT('',(-0.32,-3.29597460435593E-17,-3.91886975727153E-17));
#7347=CARTESIAN_POINT('Origin',(0.,0.,0.));
#7348=CARTESIAN_POINT('',(-0.335,0.0149999999999999,-4.10256677714363E-17));
#7349=CARTESIAN_POINT('Origin',(0.22,0.,0.));
#7350=CARTESIAN_POINT('',(-0.22,-6.93889390390723E-18,-2.69422295812418E-17));
#7351=CARTESIAN_POINT('Origin',(0.,0.,0.));
#7352=CARTESIAN_POINT('Origin',(0.,-0.02,0.));
#7353=CARTESIAN_POINT('',(-0.1954,-0.0492,2.39295984553393E-17));
#7354=CARTESIAN_POINT('Origin',(0.,-0.0492,0.));
#7355=CARTESIAN_POINT('',(-0.21,-0.02,-2.57175827820944E-17));
#7356=CARTESIAN_POINT('Origin',(0.,-0.8,0.));
#7357=CARTESIAN_POINT('',(-0.1954,-0.8,-2.39295984553393E-17));
#7394=UNCERTAINTY_MEASURE_WITH_UNIT(LENGTH_MEASURE(0.001),#7426,
'DISTANCE_ACCURACY_VALUE',
'Maximum model space distance between geometric entities at asserted c
onnectivities');
#7395=UNCERTAINTY_MEASURE_WITH_UNIT(LENGTH_MEASURE(0.001),#7426,
'DISTANCE_ACCURACY_VALUE',
'Maximum model space distance between geometric entities at asserted c
onnectivities');
#7424=(
GEOMETRIC_REPRESENTATION_CONTEXT(3)
GLOBAL_UNCERTAINTY_ASSIGNED_CONTEXT((#7394))
GLOBAL_UNIT_ASSIGNED_CONTEXT((#7426,#7428,#7429))
REPRESENTATION_CONTEXT('','3D')
);
#7425=(
GEOMETRIC_REPRESENTATION_CONTEXT(3)
GLOBAL_UNCERTAINTY_ASSIGNED_CONTEXT((#7395))
GLOBAL_UNIT_ASSIGNED_CONTEXT((#7426,#7428,#7429))
REPRESENTATION_CONTEXT('','3D')
);
#7426=(
LENGTH_UNIT()
NAMED_UNIT(*)
SI_UNIT(.CENTI.,.METRE.)
);
#7428=(
NAMED_UNIT(*)
PLANE_ANGLE_UNIT()
SI_UNIT($,.RADIAN.)
);
#7429=(
NAMED_UNIT(*)
SI_UNIT($,.STERADIAN.)
SOLID_ANGLE_UNIT()
);
#7458=SHAPE_DEFINITION_REPRESENTATION(#7524,#7561);
#7524=PRODUCT_DEFINITION_SHAPE('',$,#7591);
#7561=SHAPE_REPRESENTATION('',(#4864),#7424);
#7562=PRODUCT_DEFINITION_CONTEXT('part definition',#7651,'design');
#7591=PRODUCT_DEFINITION('M4x10 Cap Screw','M4x10 Cap Screw',#7620,#7562);
#7620=PRODUCT_DEFINITION_FORMATION('',$,#7681);
#7651=APPLICATION_CONTEXT(
'Core Data for Automotive Mechanical Design Process');
#7652=PRODUCT_CONTEXT('part definition',#7651,'mechanical');
#7681=PRODUCT('M4x10 Cap Screw','M4x10 Cap Screw','M4x10 Cap Screw',(#7652));
#7745=COLOUR_RGB('Black',0.12,0.14,0.17);
#7746=FILL_AREA_STYLE_COLOUR('',#7745);
#7747=FILL_AREA_STYLE('',(#7746));
#7748=SURFACE_STYLE_FILL_AREA(#7747);
#7749=SURFACE_SIDE_STYLE('',(#7748));
#7750=SURFACE_STYLE_USAGE(.BOTH.,#7749);
#7751=PRESENTATION_STYLE_ASSIGNMENT((#7750));
ENDSEC;
END-ISO-10303-21;
